ISO-10303-21;
HEADER;
FILE_DESCRIPTION (('STEP AP214'),
    '1' );
FILE_NAME ('Washer.step',
    '2026-10-06T10:59:17',
    ( '' ),
    ( '' ),
    'SwSTEP 2.0',
    'SolidWorks 2026',
    '' );
FILE_SCHEMA (( 'AUTOMOTIVE_DESIGN' ));
ENDSEC;

DATA;
#4=VECTOR ( 'NONE', #1471, 1000.000000000000000 ) ;
#32=PRODUCT_DEFINITION_FORMATION_WITH_SPECIFIED_SOURCE ( 'ANY', '', #540, .NOT_KNOWN. ) ;
#35=ORIENTED_EDGE ( 'NONE', *, *, #1554, .F. ) ;
#65=CIRCLE ( 'NONE', #13313, 4.200000000000000178 ) ;
#69=CIRCLE ( 'NONE', #12653, 8.199999999999999289 ) ;
#230=DIRECTION ( 'NONE',  ( 1.134288711164059445E-16, 1.000000000000000000, 7.183611964723549989E-17 ) ) ;
#255=ORIENTED_EDGE ( 'NONE', *, *, #13064, .T. ) ;
#365=CARTESIAN_POINT ( 'NONE',  ( -1.677846259693482001, 44.16218137147969003, 56.15433879953099705 ) ) ;
#381=AXIS2_PLACEMENT_3D ( 'NONE', #1625, #19694, #14599 ) ;
#388=ORIENTED_EDGE ( 'NONE', *, *, #1554, .T. ) ;
#392=ORIENTED_EDGE ( 'NONE', *, *, #17307, .F. ) ;
#533=DIRECTION ( 'NONE',  ( 3.893792155548169402E-16, 7.183611964723547524E-17, -1.000000000000000000 ) ) ;
#540=PRODUCT ( 'Washer', 'Washer', '', ( #5689 ) ) ;
#554=DIRECTION ( 'NONE',  ( 3.893792155548169402E-16, 7.183611964723547524E-17, -1.000000000000000000 ) ) ;
#577=ORIENTED_EDGE ( 'NONE', *, *, #17193, .T. ) ;
#791=VERTEX_POINT ( 'NONE', #19512 ) ;
#852=PRODUCT_DEFINITION_CONTEXT ( 'detailed design', #2327, 'design' ) ;
#956=ORIENTED_EDGE ( 'NONE', *, *, #20825, .F. ) ;
#998=AXIS2_PLACEMENT_3D ( 'NONE', #18909, #10848, #17317 ) ;
#1008=DIRECTION ( 'NONE',  ( 1.000000000000000000, 0.000000000000000000, 0.000000000000000000 ) ) ;
#1159=DIRECTION ( 'NONE',  ( 1.000000000000000000, 0.000000000000000000, 0.000000000000000000 ) ) ;
#1209=EDGE_LOOP ( 'NONE', ( #19382, #9526, #13523, #2331, #4212, #956 ) ) ;
#1283=EDGE_CURVE ( 'NONE', #6065, #4311, #16767, .T. ) ;
#1288=AXIS2_PLACEMENT_3D ( 'NONE', #16842, #4059, #3469 ) ;
#1316=CIRCLE ( 'NONE', #3006, 4.200000000000000178 ) ;
#1413=EDGE_CURVE ( 'NONE', #17717, #18484, #8482, .T. ) ;
#1471=DIRECTION ( 'NONE',  ( 3.893792155548169402E-16, 7.183611964723547524E-17, -1.000000000000000000 ) ) ;
#1529=ORIENTED_EDGE ( 'NONE', *, *, #17457, .F. ) ;
#1540=FACE_OUTER_BOUND ( 'NONE', #7776, .T. ) ;
#1554=EDGE_CURVE ( 'NONE', #14425, #6065, #15702, .T. ) ;
#1562=CARTESIAN_POINT ( 'NONE',  ( 2.722153740306517911, 44.16218137147969003, 56.15433879953099705 ) ) ;
#1570=LINE ( 'NONE', #5057, #7701 ) ;
#1625=CARTESIAN_POINT ( 'NONE',  ( 0.5221537403065181771, 44.16218137147969003, 56.15433879953099705 ) ) ;
#1632=ORIENTED_EDGE ( 'NONE', *, *, #18972, .F. ) ;
#1658=DIRECTION ( 'NONE',  ( 1.134288711164059445E-16, 1.000000000000000000, 7.183611964723549989E-17 ) ) ;
#1710=CLOSED_SHELL ( 'NONE', ( #6618, #7033, #20532, #5509, #19337, #2964, #5868, #9510, #12390, #11712, #10881, #5277 ) ) ;
#1717=CARTESIAN_POINT ( 'NONE',  ( -4.477846259693478714, 37.66295064777091994, 54.55433879953098852 ) ) ;
#1734=AXIS2_PLACEMENT_3D ( 'NONE', #16275, #19457, #9588 ) ;
#1756=ORIENTED_EDGE ( 'NONE', *, *, #20011, .F. ) ;
#1882=DIRECTION ( 'NONE',  ( -3.893792155548169402E-16, -7.183611964723547524E-17, 1.000000000000000000 ) ) ;
#1972=PRESENTATION_STYLE_ASSIGNMENT (( #19731 ) ) ;
#1999=VECTOR ( 'NONE', #2801, 1000.000000000000000 ) ;
#2016=AXIS2_PLACEMENT_3D ( 'NONE', #14834, #16545, #8247 ) ;
#2033=DIRECTION ( 'NONE',  ( 1.000000000000000000, 0.000000000000000000, 0.000000000000000000 ) ) ;
#2187=DIRECTION ( 'NONE',  ( 1.110223024625156294E-16, -1.000000000000000000, -7.183611964723542594E-17 ) ) ;
#2240=CARTESIAN_POINT ( 'NONE',  ( 0.5221537403065188432, 44.16218137147969003, 54.55433879953099563 ) ) ;
#2291=AXIS2_PLACEMENT_3D ( 'NONE', #11494, #13290, #6360 ) ;
#2327=APPLICATION_CONTEXT ( 'automotive_design' ) ;
#2331=ORIENTED_EDGE ( 'NONE', *, *, #8190, .F. ) ;
#2481=FACE_OUTER_BOUND ( 'NONE', #5850, .T. ) ;
#2498=ORIENTED_EDGE ( 'NONE', *, *, #7498, .F. ) ;
#2512=CARTESIAN_POINT ( 'NONE',  ( 2.722153740306518799, 44.16218137147969003, 54.55433879953099563 ) ) ;
#2801=DIRECTION ( 'NONE',  ( 3.893792155548169402E-16, 7.183611964723547524E-17, -1.000000000000000000 ) ) ;
#2826=EDGE_CURVE ( 'NONE', #3959, #17717, #5726, .T. ) ;
#2861=DIRECTION ( 'NONE',  ( -3.893792155548169402E-16, -7.183611964723547524E-17, 1.000000000000000000 ) ) ;
#2869=DIRECTION ( 'NONE',  ( 1.000000000000000000, 0.000000000000000000, 0.000000000000000000 ) ) ;
#2961=CARTESIAN_POINT ( 'NONE',  ( 2.722153740306517911, 44.16218137147969003, 56.15433879953099705 ) ) ;
#2964=ADVANCED_FACE ( 'NONE', ( #3372, #16160 ), #8065, .F. ) ;
#2994=VECTOR ( 'NONE', #12633, 1000.000000000000000 ) ;
#3006=AXIS2_PLACEMENT_3D ( 'NONE', #4501, #7913, #17283 ) ;
#3009=EDGE_LOOP ( 'NONE', ( #14530, #10640, #12792 ) ) ;
#3061=DIRECTION ( 'NONE',  ( 1.000000000000000000, 0.000000000000000000, 0.000000000000000000 ) ) ;
#3093=LINE ( 'NONE', #5963, #12965 ) ;
#3372=FACE_BOUND ( 'NONE', #3487, .T. ) ;
#3389=CIRCLE ( 'NONE', #13935, 8.199999999999999289 ) ;
#3469=DIRECTION ( 'NONE',  ( 1.134288711164059445E-16, 1.000000000000000000, 7.183611964723549989E-17 ) ) ;
#3474=DIRECTION ( 'NONE',  ( 3.893792155548169402E-16, 7.183611964723547524E-17, -1.000000000000000000 ) ) ;
#3487=EDGE_LOOP ( 'NONE', ( #8598, #18899, #4210, #16635, #9824, #11739 ) ) ;
#3676=( NAMED_UNIT ( * ) PLANE_ANGLE_UNIT ( ) SI_UNIT ( $, .RADIAN. ) );
#3744=CARTESIAN_POINT ( 'NONE',  ( -1.677846259693481112, 47.73989013547935656, 54.55433879953098852 ) ) ;
#3768=SURFACE_SIDE_STYLE ('',( #5468 ) ) ;
#3813=VECTOR ( 'NONE', #17344, 1000.000000000000000 ) ;
#3834=DIRECTION ( 'NONE',  ( -3.893792155548169402E-16, -7.183611964723547524E-17, 1.000000000000000000 ) ) ;
#3878=FACE_OUTER_BOUND ( 'NONE', #16014, .T. ) ;
#3933=CARTESIAN_POINT ( 'NONE',  ( 0.5221537403065191763, 44.16218137147969003, 53.55433879953099563 ) ) ;
#3959=VERTEX_POINT ( 'NONE', #5967 ) ;
#3981=DIRECTION ( 'NONE',  ( 3.893792155548169402E-16, 7.183611964723547524E-17, -1.000000000000000000 ) ) ;
#4041=CARTESIAN_POINT ( 'NONE',  ( 0.5221537403065181771, 44.16218137147969003, 56.15433879953099705 ) ) ;
#4059=DIRECTION ( 'NONE',  ( -1.000000000000000000, 1.134288711164059691E-16, -3.893792155548169402E-16 ) ) ;
#4118=CYLINDRICAL_SURFACE ( 'NONE', #11815, 4.200000000000000178 ) ;
#4160=EDGE_CURVE ( 'NONE', #14337, #18484, #19158, .T. ) ;
#4210=ORIENTED_EDGE ( 'NONE', *, *, #7498, .T. ) ;
#4212=ORIENTED_EDGE ( 'NONE', *, *, #5834, .F. ) ;
#4277=CARTESIAN_POINT ( 'NONE',  ( -1.677846259693481556, 47.73989013547935656, 56.15433879953099705 ) ) ;
#4311=VERTEX_POINT ( 'NONE', #1717 ) ;
#4316=AXIS2_PLACEMENT_3D ( 'NONE', #13268, #3474, #16151 ) ;
#4356=CARTESIAN_POINT ( 'NONE',  ( -7.677846259693480668, 44.16218137147969003, 56.15433879953099705 ) ) ;
#4361=APPLICATION_CONTEXT ( 'automotive_design' ) ;
#4428=EDGE_LOOP ( 'NONE', ( #15907, #6305, #11848, #1756 ) ) ;
#4501=CARTESIAN_POINT ( 'NONE',  ( 0.5221537403065188432, 44.16218137147969003, 54.55433879953099563 ) ) ;
#4605=MANIFOLD_SOLID_BREP ( 'Stock-MAS-160-1', #1710 ) ;
#4721=CARTESIAN_POINT ( 'NONE',  ( 8.722153740306517022, 44.16218137147969003, 56.15433879953099705 ) ) ;
#4851=LINE ( 'NONE', #11157, #4 ) ;
#4874=AXIS2_PLACEMENT_3D ( 'NONE', #11351, #15822, #13043 ) ;
#4952=FACE_OUTER_BOUND ( 'NONE', #8523, .T. ) ;
#5057=CARTESIAN_POINT ( 'NONE',  ( -1.677846259693481556, 47.73989013547935656, 56.15433879953099705 ) ) ;
#5155=AXIS2_PLACEMENT_3D ( 'NONE', #20122, #20551, #15566 ) ;
#5277=ADVANCED_FACE ( 'NONE', ( #18030 ), #14627, .T. ) ;
#5309=DIRECTION ( 'NONE',  ( 3.893792155548169402E-16, 7.183611964723547524E-17, -1.000000000000000000 ) ) ;
#5351=AXIS2_PLACEMENT_3D ( 'NONE', #4041, #12047, #8849 ) ;
#5370=( LENGTH_UNIT ( ) NAMED_UNIT ( * ) SI_UNIT ( .MILLI., .METRE. ) );
#5402=DIRECTION ( 'NONE',  ( 1.000000000000000000, 0.000000000000000000, 0.000000000000000000 ) ) ;
#5414=DIRECTION ( 'NONE',  ( 3.893792155548169402E-16, 7.183611964723547524E-17, -1.000000000000000000 ) ) ;
#5437=ORIENTED_EDGE ( 'NONE', *, *, #6256, .F. ) ;
#5468=SURFACE_STYLE_FILL_AREA ( #8682 ) ;
#5509=ADVANCED_FACE ( 'NONE', ( #7415 ), #9134, .T. ) ;
#5516=CIRCLE ( 'NONE', #20461, 4.200000000000000178 ) ;
#5637=CYLINDRICAL_SURFACE ( 'NONE', #11159, 4.200000000000000178 ) ;
#5689=PRODUCT_CONTEXT ( 'NONE', #4361, 'mechanical' ) ;
#5726=LINE ( 'NONE', #17123, #18332 ) ;
#5740=CARTESIAN_POINT ( 'NONE',  ( -4.477846259693478714, 37.66295064777091994, 53.55433879953098852 ) ) ;
#5789=VERTEX_POINT ( 'NONE', #6959 ) ;
#5834=EDGE_CURVE ( 'NONE', #13618, #17974, #15277, .T. ) ;
#5850=EDGE_LOOP ( 'NONE', ( #8113, #10368, #6357, #388 ) ) ;
#5868=ADVANCED_FACE ( 'NONE', ( #3878 ), #7290, .F. ) ;
#5963=CARTESIAN_POINT ( 'NONE',  ( -3.677846259693482445, 44.16218137147969003, 56.15433879953099705 ) ) ;
#5967=CARTESIAN_POINT ( 'NONE',  ( -7.677846259693479780, 44.16218137147969003, 53.55433879953099563 ) ) ;
#6065=VERTEX_POINT ( 'NONE', #14300 ) ;
#6082=CARTESIAN_POINT ( 'NONE',  ( 2.722153740306517911, 49.95873206995546667, 56.15433879953099705 ) ) ;
#6131=LINE ( 'NONE', #1562, #2994 ) ;
#6256=EDGE_CURVE ( 'NONE', #8809, #13618, #10481, .T. ) ;
#6305=ORIENTED_EDGE ( 'NONE', *, *, #6256, .T. ) ;
#6327=VERTEX_POINT ( 'NONE', #3744 ) ;
#6357=ORIENTED_EDGE ( 'NONE', *, *, #19506, .F. ) ;
#6360=DIRECTION ( 'NONE',  ( 1.000000000000000000, 0.000000000000000000, 0.000000000000000000 ) ) ;
#6456=STYLED_ITEM ( 'NONE', ( #1972 ), #4605 ) ;
#6554=CYLINDRICAL_SURFACE ( 'NONE', #4316, 6.199999999999999289 ) ;
#6618=ADVANCED_FACE ( 'NONE', ( #8529 ), #5637, .F. ) ;
#6641=LINE ( 'NONE', #365, #17726 ) ;
#6697=CIRCLE ( 'NONE', #2291, 8.199999999999999289 ) ;
#6751=( NAMED_UNIT ( * ) PLANE_ANGLE_UNIT ( ) SI_UNIT ( $, .RADIAN. ) );
#6959=CARTESIAN_POINT ( 'NONE',  ( -3.677846259693482445, 44.16218137147969003, 56.15433879953099705 ) ) ;
#7026=ORIENTED_EDGE ( 'NONE', *, *, #11448, .T. ) ;
#7033=ADVANCED_FACE ( 'NONE', ( #12221 ), #4118, .F. ) ;
#7042=ORIENTED_EDGE ( 'NONE', *, *, #18825, .F. ) ;
#7085=ORIENTED_EDGE ( 'NONE', *, *, #20523, .T. ) ;
#7137=VECTOR ( 'NONE', #12678, 1000.000000000000000 ) ;
#7165=ORIENTED_EDGE ( 'NONE', *, *, #16004, .F. ) ;
#7181=CARTESIAN_POINT ( 'NONE',  ( 4.722153740306518799, 44.16218137147969003, 54.55433879953099563 ) ) ;
#7267=LINE ( 'NONE', #12175, #1999 ) ;
#7290=CYLINDRICAL_SURFACE ( 'NONE', #9538, 4.200000000000000178 ) ;
#7300=ORIENTED_EDGE ( 'NONE', *, *, #10312, .T. ) ;
#7339=LINE ( 'NONE', #5740, #3813 ) ;
#7415=FACE_OUTER_BOUND ( 'NONE', #18682, .T. ) ;
#7495=( GEOMETRIC_REPRESENTATION_CONTEXT ( 3 ) GLOBAL_UNCERTAINTY_ASSIGNED_CONTEXT ( ( #18728 ) ) GLOBAL_UNIT_ASSIGNED_CONTEXT ( ( #5370, #3676, #16465 ) ) REPRESENTATION_CONTEXT ( 'NONE', 'WORKASPACE' ) );
#7498=EDGE_CURVE ( 'NONE', #5789, #16992, #8436, .T. ) ;
#7559=DIRECTION ( 'NONE',  ( 3.893792155548169402E-16, 7.183611964723547524E-17, -1.000000000000000000 ) ) ;
#7608=ORIENTED_EDGE ( 'NONE', *, *, #10312, .F. ) ;
#7657=CARTESIAN_POINT ( 'NONE',  ( 0.5221537403065188432, 44.16218137147969003, 54.55433879953099563 ) ) ;
#7701=VECTOR ( 'NONE', #1882, 1000.000000000000000 ) ;
#7733=VECTOR ( 'NONE', #5414, 1000.000000000000000 ) ;
#7776=EDGE_LOOP ( 'NONE', ( #1632, #13286, #7085, #12104, #7165, #10205 ) ) ;
#7829=ORIENTED_EDGE ( 'NONE', *, *, #20523, .F. ) ;
#7863=PLANE ( 'NONE',  #8904 ) ;
#7879=EDGE_CURVE ( 'NONE', #8809, #10514, #6131, .T. ) ;
#7913=DIRECTION ( 'NONE',  ( 3.893792155548169402E-16, 7.183611964723547524E-17, -1.000000000000000000 ) ) ;
#8023=ORIENTED_EDGE ( 'NONE', *, *, #12875, .F. ) ;
#8025=CYLINDRICAL_SURFACE ( 'NONE', #17999, 8.199999999999999289 ) ;
#8065=PLANE ( 'NONE',  #14598 ) ;
#8113=ORIENTED_EDGE ( 'NONE', *, *, #1283, .T. ) ;
#8190=EDGE_CURVE ( 'NONE', #17974, #20326, #1316, .T. ) ;
#8220=VERTEX_POINT ( 'NONE', #10046 ) ;
#8247=DIRECTION ( 'NONE',  ( 1.000000000000000000, -4.930380657631323784E-32, 3.893792155548169402E-16 ) ) ;
#8411=ORIENTED_EDGE ( 'NONE', *, *, #20011, .T. ) ;
#8436=CIRCLE ( 'NONE', #5351, 4.200000000000000178 ) ;
#8482=CIRCLE ( 'NONE', #21028, 8.199999999999999289 ) ;
#8523=EDGE_LOOP ( 'NONE', ( #18982, #5437, #1529, #18520 ) ) ;
#8529=FACE_OUTER_BOUND ( 'NONE', #19630, .T. ) ;
#8530=DIRECTION ( 'NONE',  ( -1.000000000000000000, 0.000000000000000000, 0.000000000000000000 ) ) ;
#8583=AXIS2_PLACEMENT_3D ( 'NONE', #2240, #5309, #10240 ) ;
#8598=ORIENTED_EDGE ( 'NONE', *, *, #18825, .T. ) ;
#8642=ORIENTED_EDGE ( 'NONE', *, *, #16004, .T. ) ;
#8682=FILL_AREA_STYLE ('',( #10395 ) ) ;
#8748=LINE ( 'NONE', #15132, #16022 ) ;
#8796=EDGE_CURVE ( 'NONE', #9334, #10505, #7267, .T. ) ;
#8809=VERTEX_POINT ( 'NONE', #6082 ) ;
#8822=CARTESIAN_POINT ( 'NONE',  ( 2.722153740306518799, 49.95873206995546667, 54.55433879953099563 ) ) ;
#8849=DIRECTION ( 'NONE',  ( 1.000000000000000000, 0.000000000000000000, 0.000000000000000000 ) ) ;
#8904=AXIS2_PLACEMENT_3D ( 'NONE', #2961, #14351, #9574 ) ;
#8937=CARTESIAN_POINT ( 'NONE',  ( 0.5221537403065188432, 44.16218137147969003, 54.55433879953099563 ) ) ;
#9108=DIRECTION ( 'NONE',  ( 3.620524460287510065E-17, -1.000000000000000000, -7.183611964723545059E-17 ) ) ;
#9134=CYLINDRICAL_SURFACE ( 'NONE', #998, 8.199999999999999289 ) ;
#9334=VERTEX_POINT ( 'NONE', #12947 ) ;
#9510=ADVANCED_FACE ( 'NONE', ( #18540 ), #18643, .F. ) ;
#9526=ORIENTED_EDGE ( 'NONE', *, *, #13270, .F. ) ;
#9538=AXIS2_PLACEMENT_3D ( 'NONE', #17186, #3981, #12191 ) ;
#9574=DIRECTION ( 'NONE',  ( 3.620524460287508833E-17, -1.000000000000000000, -7.183611964723545059E-17 ) ) ;
#9588=DIRECTION ( 'NONE',  ( 1.000000000000000000, 0.000000000000000000, 0.000000000000000000 ) ) ;
#9593=DIRECTION ( 'NONE',  ( 3.893792155548169402E-16, 7.183611964723547524E-17, -1.000000000000000000 ) ) ;
#9641=CARTESIAN_POINT ( 'NONE',  ( 0.5221537403065181771, 44.16218137147969003, 56.15433879953099705 ) ) ;
#9781=DIRECTION ( 'NONE',  ( 1.000000000000000000, -4.930380657631323784E-32, 3.893792155548169402E-16 ) ) ;
#9824=ORIENTED_EDGE ( 'NONE', *, *, #17457, .T. ) ;
#9886=( GEOMETRIC_REPRESENTATION_CONTEXT ( 3 ) GLOBAL_UNCERTAINTY_ASSIGNED_CONTEXT ( ( #10250 ) ) GLOBAL_UNIT_ASSIGNED_CONTEXT ( ( #10286, #6751, #11669 ) ) REPRESENTATION_CONTEXT ( 'NONE', 'WORKASPACE' ) );
#9926=AXIS2_PLACEMENT_3D ( 'NONE', #19824, #18031, #9964 ) ;
#9940=LINE ( 'NONE', #14808, #20094 ) ;
#9964=DIRECTION ( 'NONE',  ( 1.000000000000000000, 0.000000000000000000, 0.000000000000000000 ) ) ;
#10024=PLANE ( 'NONE',  #8583 ) ;
#10046=CARTESIAN_POINT ( 'NONE',  ( -4.477846259693478714, 37.66295064777091994, 53.55433879953098852 ) ) ;
#10123=ORIENTED_EDGE ( 'NONE', *, *, #4160, .F. ) ;
#10177=ORIENTED_EDGE ( 'NONE', *, *, #17821, .T. ) ;
#10205=ORIENTED_EDGE ( 'NONE', *, *, #17583, .T. ) ;
#10240=DIRECTION ( 'NONE',  ( 1.000000000000000000, -4.930380657631323784E-32, 3.893792155548169402E-16 ) ) ;
#10250=UNCERTAINTY_MEASURE_WITH_UNIT (LENGTH_MEASURE( 1.000000000000000082E-05 ), #10286, 'distance_accuracy_value', 'NONE');
#10286=( LENGTH_UNIT ( ) NAMED_UNIT ( * ) SI_UNIT ( .MILLI., .METRE. ) );
#10312=EDGE_CURVE ( 'NONE', #6327, #16992, #1570, .T. ) ;
#10351=FACE_BOUND ( 'NONE', #1209, .T. ) ;
#10368=ORIENTED_EDGE ( 'NONE', *, *, #17583, .F. ) ;
#10379=ADVANCED_BREP_SHAPE_REPRESENTATION ( '', ( #4605, #18366 ), #7495 ) ;
#10395=FILL_AREA_STYLE_COLOUR ( '', #19717 ) ;
#10481=LINE ( 'NONE', #16947, #13266 ) ;
#10505=VERTEX_POINT ( 'NONE', #20581 ) ;
#10514=VERTEX_POINT ( 'NONE', #13885 ) ;
#10640=ORIENTED_EDGE ( 'NONE', *, *, #18075, .T. ) ;
#10848=DIRECTION ( 'NONE',  ( -3.893792155548169402E-16, -7.183611964723547524E-17, 1.000000000000000000 ) ) ;
#10881=ADVANCED_FACE ( 'NONE', ( #2481 ), #12274, .F. ) ;
#11111=ORIENTED_EDGE ( 'NONE', *, *, #11448, .F. ) ;
#11157=CARTESIAN_POINT ( 'NONE',  ( 2.722153740306517911, 47.73989013547934945, 56.15433879953099705 ) ) ;
#11159=AXIS2_PLACEMENT_3D ( 'NONE', #17031, #533, #2033 ) ;
#11215=EDGE_CURVE ( 'NONE', #12777, #20326, #13510, .T. ) ;
#11351=CARTESIAN_POINT ( 'NONE',  ( 0.5221537403065188432, 44.16218137147969003, 54.55433879953099563 ) ) ;
#11381=CARTESIAN_POINT ( 'NONE',  ( 0.5221537403065181771, 44.16218137147969003, 56.15433879953099705 ) ) ;
#11448=EDGE_CURVE ( 'NONE', #3959, #14425, #6697, .T. ) ;
#11494=CARTESIAN_POINT ( 'NONE',  ( 0.5221537403065191763, 44.16218137147969003, 53.55433879953099563 ) ) ;
#11537=DIRECTION ( 'NONE',  ( 1.000000000000000000, 0.000000000000000000, 0.000000000000000000 ) ) ;
#11580=CIRCLE ( 'NONE', #1734, 6.199999999999999289 ) ;
#11624=FACE_OUTER_BOUND ( 'NONE', #3009, .T. ) ;
#11669=( NAMED_UNIT ( * ) SI_UNIT ( $, .STERADIAN. ) SOLID_ANGLE_UNIT ( ) );
#11712=ADVANCED_FACE ( 'NONE', ( #4952 ), #6554, .F. ) ;
#11739=ORIENTED_EDGE ( 'NONE', *, *, #7879, .T. ) ;
#11815=AXIS2_PLACEMENT_3D ( 'NONE', #9641, #12922, #1159 ) ;
#11848=ORIENTED_EDGE ( 'NONE', *, *, #5834, .T. ) ;
#11884=SHAPE_REPRESENTATION_RELATIONSHIP ( 'NONE' , 'NONE' ,  #14198, #10379 ) ;
#11990=CIRCLE ( 'NONE', #5155, 8.199999999999999289 ) ;
#12047=DIRECTION ( 'NONE',  ( 3.893792155548169402E-16, 7.183611964723547524E-17, -1.000000000000000000 ) ) ;
#12104=ORIENTED_EDGE ( 'NONE', *, *, #2826, .F. ) ;
#12139=ORIENTED_EDGE ( 'NONE', *, *, #2826, .T. ) ;
#12163=CARTESIAN_POINT ( 'NONE',  ( -4.477846259693478714, 37.66295064777091994, 53.55433879953098852 ) ) ;
#12175=CARTESIAN_POINT ( 'NONE',  ( -1.677846259693485109, 49.95873206995546667, 56.15433879953099705 ) ) ;
#12191=DIRECTION ( 'NONE',  ( 1.000000000000000000, 0.000000000000000000, 0.000000000000000000 ) ) ;
#12221=FACE_OUTER_BOUND ( 'NONE', #18564, .T. ) ;
#12274=PLANE ( 'NONE',  #20273 ) ;
#12390=ADVANCED_FACE ( 'NONE', ( #17538 ), #7863, .F. ) ;
#12633=DIRECTION ( 'NONE',  ( 3.620524460287510065E-17, -1.000000000000000000, -7.183611964723545059E-17 ) ) ;
#12647=DIRECTION ( 'NONE',  ( 0.000000000000000000, 0.000000000000000000, 1.000000000000000000 ) ) ;
#12653=AXIS2_PLACEMENT_3D ( 'NONE', #8937, #13500, #5402 ) ;
#12678=DIRECTION ( 'NONE',  ( -3.893792155548169402E-16, -7.183611964723547524E-17, 1.000000000000000000 ) ) ;
#12777=VERTEX_POINT ( 'NONE', #15722 ) ;
#12792=ORIENTED_EDGE ( 'NONE', *, *, #18972, .T. ) ;
#12875=EDGE_CURVE ( 'NONE', #16992, #9334, #6641, .T. ) ;
#12922=DIRECTION ( 'NONE',  ( 3.893792155548169402E-16, 7.183611964723547524E-17, -1.000000000000000000 ) ) ;
#12947=CARTESIAN_POINT ( 'NONE',  ( -1.677846259693485109, 49.95873206995546667, 56.15433879953099705 ) ) ;
#12965=VECTOR ( 'NONE', #9593, 1000.000000000000000 ) ;
#13028=ORIENTED_EDGE ( 'NONE', *, *, #8190, .T. ) ;
#13043=DIRECTION ( 'NONE',  ( 1.000000000000000000, 0.000000000000000000, 0.000000000000000000 ) ) ;
#13059=CIRCLE ( 'NONE', #4874, 4.200000000000000178 ) ;
#13064=EDGE_CURVE ( 'NONE', #6327, #10505, #9940, .T. ) ;
#13262=CARTESIAN_POINT ( 'NONE',  ( -4.477846259693478714, 37.66295064777091994, 54.55433879953098852 ) ) ;
#13266=VECTOR ( 'NONE', #13540, 1000.000000000000000 ) ;
#13268=CARTESIAN_POINT ( 'NONE',  ( 0.5221537403065181771, 44.16218137147969003, 56.15433879953099705 ) ) ;
#13270=EDGE_CURVE ( 'NONE', #791, #6327, #65, .T. ) ;
#13286=ORIENTED_EDGE ( 'NONE', *, *, #4160, .T. ) ;
#13290=DIRECTION ( 'NONE',  ( 3.893792155548169402E-16, 7.183611964723547524E-17, -1.000000000000000000 ) ) ;
#13313=AXIS2_PLACEMENT_3D ( 'NONE', #7657, #14239, #2869 ) ;
#13317=ORIENTED_EDGE ( 'NONE', *, *, #17821, .F. ) ;
#13406=CARTESIAN_POINT ( 'NONE',  ( 2.722153740306518799, 47.73989013547934945, 54.55433879953099563 ) ) ;
#13456=PRODUCT_DEFINITION_SHAPE ( 'NONE', 'NONE',  #17682 ) ;
#13500=DIRECTION ( 'NONE',  ( 3.893792155548169402E-16, 7.183611964723547524E-17, -1.000000000000000000 ) ) ;
#13510=LINE ( 'NONE', #19987, #7733 ) ;
#13523=ORIENTED_EDGE ( 'NONE', *, *, #17193, .F. ) ;
#13540=DIRECTION ( 'NONE',  ( 3.893792155548169402E-16, 7.183611964723547524E-17, -1.000000000000000000 ) ) ;
#13570=SHAPE_DEFINITION_REPRESENTATION ( #13456, #14198 ) ;
#13618=VERTEX_POINT ( 'NONE', #8822 ) ;
#13678=ORIENTED_EDGE ( 'NONE', *, *, #11215, .T. ) ;
#13691=ORIENTED_EDGE ( 'NONE', *, *, #11215, .F. ) ;
#13885=CARTESIAN_POINT ( 'NONE',  ( 2.722153740306517911, 47.73989013547934945, 56.15433879953099705 ) ) ;
#13935=AXIS2_PLACEMENT_3D ( 'NONE', #17598, #17706, #16120 ) ;
#13996=ORIENTED_EDGE ( 'NONE', *, *, #13270, .T. ) ;
#14198=SHAPE_REPRESENTATION ( 'Washer', ( #18366 ), #7495 ) ;
#14239=DIRECTION ( 'NONE',  ( 3.893792155548169402E-16, 7.183611964723547524E-17, -1.000000000000000000 ) ) ;
#14300=CARTESIAN_POINT ( 'NONE',  ( -4.477846259693480491, 50.66141209518846011, 54.55433879953098852 ) ) ;
#14337=VERTEX_POINT ( 'NONE', #19453 ) ;
#14351=DIRECTION ( 'NONE',  ( 1.000000000000000000, 3.620524460287505751E-17, 3.893792155548169402E-16 ) ) ;
#14404=CARTESIAN_POINT ( 'NONE',  ( 0.5221537403065181771, 44.16218137147969003, 56.15433879953099705 ) ) ;
#14425=VERTEX_POINT ( 'NONE', #18191 ) ;
#14511=CARTESIAN_POINT ( 'NONE',  ( 0.5221537403065188432, 44.16218137147969003, 54.55433879953099563 ) ) ;
#14530=ORIENTED_EDGE ( 'NONE', *, *, #1283, .F. ) ;
#14598=AXIS2_PLACEMENT_3D ( 'NONE', #11381, #17851, #9781 ) ;
#14599=DIRECTION ( 'NONE',  ( 1.000000000000000000, 0.000000000000000000, 0.000000000000000000 ) ) ;
#14627=PLANE ( 'NONE',  #2016 ) ;
#14808=CARTESIAN_POINT ( 'NONE',  ( -1.677846259693481556, 44.16218137147969003, 54.55433879953098852 ) ) ;
#14834=CARTESIAN_POINT ( 'NONE',  ( 0.5221537403065191763, 44.16218137147969003, 53.55433879953099563 ) ) ;
#15132=CARTESIAN_POINT ( 'NONE',  ( -4.477846259693478714, 37.66295064777091994, 53.55433879953098852 ) ) ;
#15277=LINE ( 'NONE', #2512, #20026 ) ;
#15336=DIRECTION ( 'NONE',  ( 1.000000000000000000, 0.000000000000000000, 0.000000000000000000 ) ) ;
#15358=DIRECTION ( 'NONE',  ( -1.000000000000000000, 4.930380657631323784E-32, -3.893792155548169402E-16 ) ) ;
#15447=DIRECTION ( 'NONE',  ( -3.893792155548169402E-16, -7.183611964723547524E-17, 1.000000000000000000 ) ) ;
#15566=DIRECTION ( 'NONE',  ( 1.000000000000000000, 0.000000000000000000, 0.000000000000000000 ) ) ;
#15593=CARTESIAN_POINT ( 'NONE',  ( 0.5221537403065181771, 44.16218137147969003, 56.15433879953099705 ) ) ;
#15595=ORIENTED_EDGE ( 'NONE', *, *, #18075, .F. ) ;
#15702=LINE ( 'NONE', #18984, #17973 ) ;
#15722=CARTESIAN_POINT ( 'NONE',  ( 4.722153740306518799, 44.16218137147969003, 56.15433879953099705 ) ) ;
#15822=DIRECTION ( 'NONE',  ( 3.893792155548169402E-16, 7.183611964723547524E-17, -1.000000000000000000 ) ) ;
#15907=ORIENTED_EDGE ( 'NONE', *, *, #7879, .F. ) ;
#16004=EDGE_CURVE ( 'NONE', #8220, #3959, #16430, .T. ) ;
#16014=EDGE_LOOP ( 'NONE', ( #13691, #7042, #8411, #13028 ) ) ;
#16022=VECTOR ( 'NONE', #15447, 1000.000000000000000 ) ;
#16120=DIRECTION ( 'NONE',  ( 1.000000000000000000, 0.000000000000000000, 0.000000000000000000 ) ) ;
#16151=DIRECTION ( 'NONE',  ( 1.000000000000000000, 0.000000000000000000, 0.000000000000000000 ) ) ;
#16153=CARTESIAN_POINT ( 'NONE',  ( 0.000000000000000000, 0.000000000000000000, 0.000000000000000000 ) ) ;
#16160=FACE_OUTER_BOUND ( 'NONE', #16259, .T. ) ;
#16259=EDGE_LOOP ( 'NONE', ( #19282, #7829 ) ) ;
#16275=CARTESIAN_POINT ( 'NONE',  ( 0.5221537403065188432, 44.16218137147969003, 54.55433879953099563 ) ) ;
#16430=CIRCLE ( 'NONE', #19808, 8.199999999999999289 ) ;
#16465=( NAMED_UNIT ( * ) SI_UNIT ( $, .STERADIAN. ) SOLID_ANGLE_UNIT ( ) );
#16545=DIRECTION ( 'NONE',  ( 3.893792155548169402E-16, 7.183611964723547524E-17, -1.000000000000000000 ) ) ;
#16635=ORIENTED_EDGE ( 'NONE', *, *, #12875, .T. ) ;
#16767=LINE ( 'NONE', #13262, #17996 ) ;
#16842=CARTESIAN_POINT ( 'NONE',  ( -1.677846259693482001, 44.16218137147969003, 56.15433879953099705 ) ) ;
#16947=CARTESIAN_POINT ( 'NONE',  ( 2.722153740306517911, 49.95873206995546667, 56.15433879953099705 ) ) ;
#16992=VERTEX_POINT ( 'NONE', #4277 ) ;
#17031=CARTESIAN_POINT ( 'NONE',  ( 0.5221537403065181771, 44.16218137147969003, 56.15433879953099705 ) ) ;
#17035=CIRCLE ( 'NONE', #381, 6.199999999999999289 ) ;
#17084=DIRECTION ( 'NONE',  ( 3.893792155548169402E-16, 7.183611964723547524E-17, -1.000000000000000000 ) ) ;
#17123=CARTESIAN_POINT ( 'NONE',  ( -7.677846259693480668, 44.16218137147969003, 54.55433879953099563 ) ) ;
#17186=CARTESIAN_POINT ( 'NONE',  ( 0.5221537403065181771, 44.16218137147969003, 56.15433879953099705 ) ) ;
#17193=EDGE_CURVE ( 'NONE', #20326, #791, #13059, .T. ) ;
#17283=DIRECTION ( 'NONE',  ( 1.000000000000000000, 0.000000000000000000, 0.000000000000000000 ) ) ;
#17307=EDGE_CURVE ( 'NONE', #12777, #5789, #18396, .T. ) ;
#17317=DIRECTION ( 'NONE',  ( -1.000000000000000000, 0.000000000000000000, 0.000000000000000000 ) ) ;
#17344=DIRECTION ( 'NONE',  ( 1.110223024625156294E-16, -1.000000000000000000, -7.183611964723542594E-17 ) ) ;
#17457=EDGE_CURVE ( 'NONE', #9334, #8809, #17035, .T. ) ;
#17538=FACE_OUTER_BOUND ( 'NONE', #4428, .T. ) ;
#17583=EDGE_CURVE ( 'NONE', #8220, #4311, #8748, .T. ) ;
#17592=DIRECTION ( 'NONE',  ( 3.893792155548169402E-16, 7.183611964723547524E-17, -1.000000000000000000 ) ) ;
#17598=CARTESIAN_POINT ( 'NONE',  ( 0.5221537403065181771, 44.16218137147969003, 56.15433879953099705 ) ) ;
#17682=PRODUCT_DEFINITION ( 'UNKNOWN', '', #32, #852 ) ;
#17704=ORIENTED_EDGE ( 'NONE', *, *, #19506, .T. ) ;
#17706=DIRECTION ( 'NONE',  ( 3.893792155548169402E-16, 7.183611964723547524E-17, -1.000000000000000000 ) ) ;
#17717=VERTEX_POINT ( 'NONE', #4356 ) ;
#17726=VECTOR ( 'NONE', #1658, 1000.000000000000000 ) ;
#17821=EDGE_CURVE ( 'NONE', #5789, #791, #3093, .T. ) ;
#17851=DIRECTION ( 'NONE',  ( 3.893792155548169402E-16, 7.183611964723547524E-17, -1.000000000000000000 ) ) ;
#17928=ORIENTED_EDGE ( 'NONE', *, *, #8796, .F. ) ;
#17973=VECTOR ( 'NONE', #20972, 1000.000000000000000 ) ;
#17974=VERTEX_POINT ( 'NONE', #13406 ) ;
#17996=VECTOR ( 'NONE', #2187, 1000.000000000000000 ) ;
#17999=AXIS2_PLACEMENT_3D ( 'NONE', #14511, #3834, #8530 ) ;
#18030=FACE_OUTER_BOUND ( 'NONE', #20359, .T. ) ;
#18031=DIRECTION ( 'NONE',  ( 3.893792155548169402E-16, 7.183611964723547524E-17, -1.000000000000000000 ) ) ;
#18075=EDGE_CURVE ( 'NONE', #6065, #14337, #69, .T. ) ;
#18191=CARTESIAN_POINT ( 'NONE',  ( -4.477846259693480491, 50.66141209518846011, 53.55433879953099563 ) ) ;
#18332=VECTOR ( 'NONE', #2861, 1000.000000000000000 ) ;
#18357=MECHANICAL_DESIGN_GEOMETRIC_PRESENTATION_REPRESENTATION('',(#6456),#9886);
#18366=AXIS2_PLACEMENT_3D ( 'NONE', #16153, #12647, #3061 ) ;
#18396=CIRCLE ( 'NONE', #9926, 4.200000000000000178 ) ;
#18484=VERTEX_POINT ( 'NONE', #4721 ) ;
#18520=ORIENTED_EDGE ( 'NONE', *, *, #8796, .T. ) ;
#18540=FACE_OUTER_BOUND ( 'NONE', #20058, .T. ) ;
#18564=EDGE_LOOP ( 'NONE', ( #13317, #392, #13678, #577 ) ) ;
#18643=PLANE ( 'NONE',  #1288 ) ;
#18682=EDGE_LOOP ( 'NONE', ( #10123, #15595, #35, #11111, #12139, #20895 ) ) ;
#18728=UNCERTAINTY_MEASURE_WITH_UNIT (LENGTH_MEASURE( 1.000000000000000082E-05 ), #5370, 'distance_accuracy_value', 'NONE');
#18825=EDGE_CURVE ( 'NONE', #10514, #12777, #5516, .T. ) ;
#18899=ORIENTED_EDGE ( 'NONE', *, *, #17307, .T. ) ;
#18909=CARTESIAN_POINT ( 'NONE',  ( 0.5221537403065188432, 44.16218137147969003, 54.55433879953099563 ) ) ;
#18972=EDGE_CURVE ( 'NONE', #14337, #4311, #11990, .T. ) ;
#18982=ORIENTED_EDGE ( 'NONE', *, *, #20825, .T. ) ;
#18984=CARTESIAN_POINT ( 'NONE',  ( -4.477846259693480491, 50.66141209518846011, 53.55433879953099563 ) ) ;
#19062=CARTESIAN_POINT ( 'NONE',  ( 8.722153740306517022, 44.16218137147969003, 54.55433879953099563 ) ) ;
#19158=LINE ( 'NONE', #19062, #7137 ) ;
#19282=ORIENTED_EDGE ( 'NONE', *, *, #1413, .F. ) ;
#19337=ADVANCED_FACE ( 'NONE', ( #11624, #10351 ), #10024, .T. ) ;
#19382=ORIENTED_EDGE ( 'NONE', *, *, #13064, .F. ) ;
#19453=CARTESIAN_POINT ( 'NONE',  ( 8.722153740306517022, 44.16218137147969003, 54.55433879953099563 ) ) ;
#19457=DIRECTION ( 'NONE',  ( 3.893792155548169402E-16, 7.183611964723547524E-17, -1.000000000000000000 ) ) ;
#19506=EDGE_CURVE ( 'NONE', #14425, #8220, #7339, .T. ) ;
#19512=CARTESIAN_POINT ( 'NONE',  ( -3.677846259693482001, 44.16218137147969003, 54.55433879953099563 ) ) ;
#19630=EDGE_LOOP ( 'NONE', ( #2498, #10177, #13996, #7300 ) ) ;
#19694=DIRECTION ( 'NONE',  ( 3.893792155548169402E-16, 7.183611964723547524E-17, -1.000000000000000000 ) ) ;
#19717=COLOUR_RGB ( '', 0.09019608, 0.27058824, 0.51372549) ;
#19731=SURFACE_STYLE_USAGE ( .BOTH. , #3768 ) ;
#19808=AXIS2_PLACEMENT_3D ( 'NONE', #3933, #7559, #15336 ) ;
#19824=CARTESIAN_POINT ( 'NONE',  ( 0.5221537403065181771, 44.16218137147969003, 56.15433879953099705 ) ) ;
#19987=CARTESIAN_POINT ( 'NONE',  ( 4.722153740306518799, 44.16218137147969003, 56.15433879953099705 ) ) ;
#20011=EDGE_CURVE ( 'NONE', #10514, #17974, #4851, .T. ) ;
#20026=VECTOR ( 'NONE', #9108, 1000.000000000000000 ) ;
#20058=EDGE_LOOP ( 'NONE', ( #255, #17928, #8023, #7608 ) ) ;
#20094=VECTOR ( 'NONE', #230, 1000.000000000000000 ) ;
#20122=CARTESIAN_POINT ( 'NONE',  ( 0.5221537403065188432, 44.16218137147969003, 54.55433879953099563 ) ) ;
#20273=AXIS2_PLACEMENT_3D ( 'NONE', #12163, #15358, #554 ) ;
#20326=VERTEX_POINT ( 'NONE', #7181 ) ;
#20359=EDGE_LOOP ( 'NONE', ( #8642, #7026, #17704 ) ) ;
#20461=AXIS2_PLACEMENT_3D ( 'NONE', #14404, #17592, #11537 ) ;
#20523=EDGE_CURVE ( 'NONE', #18484, #17717, #3389, .T. ) ;
#20532=ADVANCED_FACE ( 'NONE', ( #1540 ), #8025, .T. ) ;
#20551=DIRECTION ( 'NONE',  ( 3.893792155548169402E-16, 7.183611964723547524E-17, -1.000000000000000000 ) ) ;
#20581=CARTESIAN_POINT ( 'NONE',  ( -1.677846259693484665, 49.95873206995546667, 54.55433879953099563 ) ) ;
#20825=EDGE_CURVE ( 'NONE', #10505, #13618, #11580, .T. ) ;
#20895=ORIENTED_EDGE ( 'NONE', *, *, #1413, .T. ) ;
#20972=DIRECTION ( 'NONE',  ( -3.893792155548169402E-16, -7.183611964723547524E-17, 1.000000000000000000 ) ) ;
#21028=AXIS2_PLACEMENT_3D ( 'NONE', #15593, #17084, #1008 ) ;
ENDSEC;
END-ISO-10303-21;
